ISO-10303-21;
HEADER;
/* Generated by software containing ST-Developer
 * from STEP Tools, Inc. (www.steptools.com) 
 */

FILE_DESCRIPTION(
/* description */ ('Guided pneumatic stop gate'),
/* implementation_level */ '2;1');

FILE_NAME(
/* name */ 'Hex Nut - M6.step',
/* time_stamp */ '2026-10-27T21:43:45-07:00',
/* author */ (''),
/* organization */ (''),
/* preprocessor_version */ 'ST-DEVELOPER v20.2',
/* originating_system */ 'Autodesk Translation Framework v15.17.0.0',
/* authorisation */ '');

FILE_SCHEMA (('AUTOMOTIVE_DESIGN { 1 0 10303 214 3 1 1 }'));
ENDSEC;

DATA;
#10=MECHANICAL_DESIGN_GEOMETRIC_PRESENTATION_REPRESENTATION('',(#576),#14392);
#31=(
BOUNDED_CURVE()
B_SPLINE_CURVE(2,(#14204,#14205,#14206),.UNSPECIFIED.,.F.,.F.)
B_SPLINE_CURVE_WITH_KNOTS((3,3),(0.144988513094728,0.791574906712449),
 .UNSPECIFIED.)
CURVE()
GEOMETRIC_REPRESENTATION_ITEM()
RATIONAL_B_SPLINE_CURVE((1.09282032302755,1.26188021535082,1.09282032302931))
REPRESENTATION_ITEM('')
);
#32=(
BOUNDED_CURVE()
B_SPLINE_CURVE(2,(#14208,#14209,#14210),.UNSPECIFIED.,.F.,.F.)
B_SPLINE_CURVE_WITH_KNOTS((3,3),(0.144988513094728,0.791574906712449),
 .UNSPECIFIED.)
CURVE()
GEOMETRIC_REPRESENTATION_ITEM()
RATIONAL_B_SPLINE_CURVE((1.09282032302755,1.26188021535082,1.09282032302931))
REPRESENTATION_ITEM('')
);
#33=(
BOUNDED_CURVE()
B_SPLINE_CURVE(2,(#14215,#14216,#14217),.UNSPECIFIED.,.F.,.F.)
B_SPLINE_CURVE_WITH_KNOTS((3,3),(0.144988513094728,0.791574906712449),
 .UNSPECIFIED.)
CURVE()
GEOMETRIC_REPRESENTATION_ITEM()
RATIONAL_B_SPLINE_CURVE((1.09282032302755,1.26188021535082,1.09282032302931))
REPRESENTATION_ITEM('')
);
#34=(
BOUNDED_CURVE()
B_SPLINE_CURVE(2,(#14219,#14220,#14221),.UNSPECIFIED.,.F.,.F.)
B_SPLINE_CURVE_WITH_KNOTS((3,3),(0.144988513094728,0.791574906712449),
 .UNSPECIFIED.)
CURVE()
GEOMETRIC_REPRESENTATION_ITEM()
RATIONAL_B_SPLINE_CURVE((1.09282032302755,1.26188021535082,1.09282032302931))
REPRESENTATION_ITEM('')
);
#35=(
BOUNDED_CURVE()
B_SPLINE_CURVE(2,(#14223,#14224,#14225),.UNSPECIFIED.,.F.,.F.)
B_SPLINE_CURVE_WITH_KNOTS((3,3),(0.144988513094728,0.791574906712449),
 .UNSPECIFIED.)
CURVE()
GEOMETRIC_REPRESENTATION_ITEM()
RATIONAL_B_SPLINE_CURVE((1.09282032302755,1.26188021535082,1.09282032302931))
REPRESENTATION_ITEM('')
);
#36=(
BOUNDED_CURVE()
B_SPLINE_CURVE(2,(#14226,#14227,#14228),.UNSPECIFIED.,.F.,.F.)
B_SPLINE_CURVE_WITH_KNOTS((3,3),(0.144988513094728,0.791574906712449),
 .UNSPECIFIED.)
CURVE()
GEOMETRIC_REPRESENTATION_ITEM()
RATIONAL_B_SPLINE_CURVE((1.09282032302755,1.26188021535082,1.09282032302931))
REPRESENTATION_ITEM('')
);
#37=(
BOUNDED_CURVE()
B_SPLINE_CURVE(2,(#14235,#14236,#14237),.UNSPECIFIED.,.F.,.F.)
B_SPLINE_CURVE_WITH_KNOTS((3,3),(0.144988513094728,0.791574906712449),
 .UNSPECIFIED.)
CURVE()
GEOMETRIC_REPRESENTATION_ITEM()
RATIONAL_B_SPLINE_CURVE((1.09282032302755,1.26188021535082,1.09282032302931))
REPRESENTATION_ITEM('')
);
#38=(
BOUNDED_CURVE()
B_SPLINE_CURVE(2,(#14239,#14240,#14241),.UNSPECIFIED.,.F.,.F.)
B_SPLINE_CURVE_WITH_KNOTS((3,3),(0.144988513094727,0.791574906712449),
 .UNSPECIFIED.)
CURVE()
GEOMETRIC_REPRESENTATION_ITEM()
RATIONAL_B_SPLINE_CURVE((1.09282032302755,1.26188021535082,1.09282032302931))
REPRESENTATION_ITEM('')
);
#39=(
BOUNDED_CURVE()
B_SPLINE_CURVE(2,(#14243,#14244,#14245),.UNSPECIFIED.,.F.,.F.)
B_SPLINE_CURVE_WITH_KNOTS((3,3),(0.144988513094728,0.791574906712449),
 .UNSPECIFIED.)
CURVE()
GEOMETRIC_REPRESENTATION_ITEM()
RATIONAL_B_SPLINE_CURVE((1.09282032302755,1.26188021535082,1.09282032302931))
REPRESENTATION_ITEM('')
);
#40=(
BOUNDED_CURVE()
B_SPLINE_CURVE(2,(#14247,#14248,#14249),.UNSPECIFIED.,.F.,.F.)
B_SPLINE_CURVE_WITH_KNOTS((3,3),(0.144988513094728,0.791574906712449),
 .UNSPECIFIED.)
CURVE()
GEOMETRIC_REPRESENTATION_ITEM()
RATIONAL_B_SPLINE_CURVE((1.09282032302755,1.26188021535082,1.09282032302931))
REPRESENTATION_ITEM('')
);
#41=(
BOUNDED_CURVE()
B_SPLINE_CURVE(2,(#14251,#14252,#14253),.UNSPECIFIED.,.F.,.F.)
B_SPLINE_CURVE_WITH_KNOTS((3,3),(0.144988513094728,0.791574906712449),
 .UNSPECIFIED.)
CURVE()
GEOMETRIC_REPRESENTATION_ITEM()
RATIONAL_B_SPLINE_CURVE((1.09282032302755,1.26188021535082,1.09282032302931))
REPRESENTATION_ITEM('')
);
#42=(
BOUNDED_CURVE()
B_SPLINE_CURVE(2,(#14254,#14255,#14256),.UNSPECIFIED.,.F.,.F.)
B_SPLINE_CURVE_WITH_KNOTS((3,3),(0.144988513094727,0.791574906712449),
 .UNSPECIFIED.)
CURVE()
GEOMETRIC_REPRESENTATION_ITEM()
RATIONAL_B_SPLINE_CURVE((1.09282032302755,1.26188021535082,1.09282032302931))
REPRESENTATION_ITEM('')
);
#449=CONICAL_SURFACE('',#9346,0.576175134594813,1.0471975511966);
#450=CONICAL_SURFACE('',#9348,0.576175134594813,1.0471975511966);
#492=SHAPE_REPRESENTATION_RELATIONSHIP('SRR','None',#14629,#534);
#534=ADVANCED_BREP_SHAPE_REPRESENTATION('',(#614),#14391);
#576=STYLED_ITEM('',(#14898),#614);
#614=MANIFOLD_SOLID_BREP('Body1',#7920);
#823=FACE_BOUND('',#2275,.T.);
#824=FACE_BOUND('',#2277,.T.);
#1110=PLANE('',#9350);
#1111=PLANE('',#9351);
#1112=PLANE('',#9352);
#1113=PLANE('',#9356);
#1114=PLANE('',#9357);
#1115=PLANE('',#9358);
#1116=PLANE('',#9359);
#1117=PLANE('',#9360);
#1582=FACE_OUTER_BOUND('',#2265,.T.);
#1583=FACE_OUTER_BOUND('',#2266,.T.);
#1584=FACE_OUTER_BOUND('',#2267,.T.);
#1585=FACE_OUTER_BOUND('',#2268,.T.);
#1586=FACE_OUTER_BOUND('',#2269,.T.);
#1587=FACE_OUTER_BOUND('',#2270,.T.);
#1588=FACE_OUTER_BOUND('',#2271,.T.);
#1589=FACE_OUTER_BOUND('',#2272,.T.);
#1590=FACE_OUTER_BOUND('',#2273,.T.);
#1591=FACE_OUTER_BOUND('',#2274,.T.);
#1592=FACE_OUTER_BOUND('',#2276,.T.);
#2265=EDGE_LOOP('',(#7186,#7187,#7188,#7189,#7190,#7191,#7192,#7193,#7194));
#2266=EDGE_LOOP('',(#7195,#7196,#7197,#7198,#7199,#7200,#7201,#7202,#7203));
#2267=EDGE_LOOP('',(#7204,#7205,#7206,#7207));
#2268=EDGE_LOOP('',(#7208,#7209,#7210,#7211));
#2269=EDGE_LOOP('',(#7212,#7213,#7214,#7215));
#2270=EDGE_LOOP('',(#7216,#7217,#7218,#7219));
#2271=EDGE_LOOP('',(#7220,#7221,#7222,#7223));
#2272=EDGE_LOOP('',(#7224,#7225,#7226,#7227));
#2273=EDGE_LOOP('',(#7228,#7229,#7230,#7231));
#2274=EDGE_LOOP('',(#7232));
#2275=EDGE_LOOP('',(#7233));
#2276=EDGE_LOOP('',(#7234));
#2277=EDGE_LOOP('',(#7235));
#2814=LINE('',#14212,#3359);
#2815=LINE('',#14233,#3360);
#2816=LINE('',#14258,#3361);
#2817=LINE('',#14259,#3362);
#2818=LINE('',#14261,#3363);
#2819=LINE('',#14263,#3364);
#2820=LINE('',#14268,#3365);
#2821=LINE('',#14271,#3366);
#2822=LINE('',#14273,#3367);
#3359=VECTOR('',#11843,0.576175134594813);
#3360=VECTOR('',#11850,0.576175134594813);
#3361=VECTOR('',#11853,1.);
#3362=VECTOR('',#11854,1.);
#3363=VECTOR('',#11857,1.);
#3364=VECTOR('',#11860,1.);
#3365=VECTOR('',#11865,0.3);
#3366=VECTOR('',#11870,1.);
#3367=VECTOR('',#11873,1.);
#3733=CIRCLE('',#9347,0.475);
#3734=CIRCLE('',#9349,0.475);
#3735=CIRCLE('',#9354,0.25175);
#3736=CIRCLE('',#9355,0.25175);
#4340=VERTEX_POINT('',#14202);
#4341=VERTEX_POINT('',#14203);
#4342=VERTEX_POINT('',#14207);
#4343=VERTEX_POINT('',#14211);
#4344=VERTEX_POINT('',#14214);
#4345=VERTEX_POINT('',#14218);
#4346=VERTEX_POINT('',#14222);
#4347=VERTEX_POINT('',#14230);
#4348=VERTEX_POINT('',#14232);
#4349=VERTEX_POINT('',#14234);
#4350=VERTEX_POINT('',#14238);
#4351=VERTEX_POINT('',#14242);
#4352=VERTEX_POINT('',#14246);
#4353=VERTEX_POINT('',#14250);
#4354=VERTEX_POINT('',#14265);
#4355=VERTEX_POINT('',#14267);
#5291=EDGE_CURVE('',#4340,#4341,#31,.T.);
#5292=EDGE_CURVE('',#4342,#4340,#32,.T.);
#5293=EDGE_CURVE('',#4342,#4343,#2814,.T.);
#5294=EDGE_CURVE('',#4343,#4343,#3733,.T.);
#5295=EDGE_CURVE('',#4344,#4342,#33,.T.);
#5296=EDGE_CURVE('',#4345,#4344,#34,.T.);
#5297=EDGE_CURVE('',#4346,#4345,#35,.T.);
#5298=EDGE_CURVE('',#4341,#4346,#36,.T.);
#5299=EDGE_CURVE('',#4347,#4347,#3734,.T.);
#5300=EDGE_CURVE('',#4347,#4348,#2815,.T.);
#5301=EDGE_CURVE('',#4349,#4348,#37,.T.);
#5302=EDGE_CURVE('',#4350,#4349,#38,.T.);
#5303=EDGE_CURVE('',#4351,#4350,#39,.T.);
#5304=EDGE_CURVE('',#4352,#4351,#40,.T.);
#5305=EDGE_CURVE('',#4353,#4352,#41,.T.);
#5306=EDGE_CURVE('',#4348,#4353,#42,.T.);
#5307=EDGE_CURVE('',#4344,#4353,#2816,.T.);
#5308=EDGE_CURVE('',#4345,#4352,#2817,.T.);
#5309=EDGE_CURVE('',#4342,#4348,#2818,.T.);
#5310=EDGE_CURVE('',#4340,#4349,#2819,.T.);
#5311=EDGE_CURVE('',#4354,#4354,#3735,.F.);
#5312=EDGE_CURVE('',#4354,#4355,#2820,.T.);
#5313=EDGE_CURVE('',#4355,#4355,#3736,.F.);
#5314=EDGE_CURVE('',#4341,#4350,#2821,.T.);
#5315=EDGE_CURVE('',#4346,#4351,#2822,.T.);
#7186=ORIENTED_EDGE('',*,*,#5291,.F.);
#7187=ORIENTED_EDGE('',*,*,#5292,.F.);
#7188=ORIENTED_EDGE('',*,*,#5293,.T.);
#7189=ORIENTED_EDGE('',*,*,#5294,.F.);
#7190=ORIENTED_EDGE('',*,*,#5293,.F.);
#7191=ORIENTED_EDGE('',*,*,#5295,.F.);
#7192=ORIENTED_EDGE('',*,*,#5296,.F.);
#7193=ORIENTED_EDGE('',*,*,#5297,.F.);
#7194=ORIENTED_EDGE('',*,*,#5298,.F.);
#7195=ORIENTED_EDGE('',*,*,#5299,.F.);
#7196=ORIENTED_EDGE('',*,*,#5300,.T.);
#7197=ORIENTED_EDGE('',*,*,#5301,.F.);
#7198=ORIENTED_EDGE('',*,*,#5302,.F.);
#7199=ORIENTED_EDGE('',*,*,#5303,.F.);
#7200=ORIENTED_EDGE('',*,*,#5304,.F.);
#7201=ORIENTED_EDGE('',*,*,#5305,.F.);
#7202=ORIENTED_EDGE('',*,*,#5306,.F.);
#7203=ORIENTED_EDGE('',*,*,#5300,.F.);
#7204=ORIENTED_EDGE('',*,*,#5296,.T.);
#7205=ORIENTED_EDGE('',*,*,#5307,.T.);
#7206=ORIENTED_EDGE('',*,*,#5305,.T.);
#7207=ORIENTED_EDGE('',*,*,#5308,.F.);
#7208=ORIENTED_EDGE('',*,*,#5295,.T.);
#7209=ORIENTED_EDGE('',*,*,#5309,.T.);
#7210=ORIENTED_EDGE('',*,*,#5306,.T.);
#7211=ORIENTED_EDGE('',*,*,#5307,.F.);
#7212=ORIENTED_EDGE('',*,*,#5292,.T.);
#7213=ORIENTED_EDGE('',*,*,#5310,.T.);
#7214=ORIENTED_EDGE('',*,*,#5301,.T.);
#7215=ORIENTED_EDGE('',*,*,#5309,.F.);
#7216=ORIENTED_EDGE('',*,*,#5311,.F.);
#7217=ORIENTED_EDGE('',*,*,#5312,.T.);
#7218=ORIENTED_EDGE('',*,*,#5313,.T.);
#7219=ORIENTED_EDGE('',*,*,#5312,.F.);
#7220=ORIENTED_EDGE('',*,*,#5291,.T.);
#7221=ORIENTED_EDGE('',*,*,#5314,.T.);
#7222=ORIENTED_EDGE('',*,*,#5302,.T.);
#7223=ORIENTED_EDGE('',*,*,#5310,.F.);
#7224=ORIENTED_EDGE('',*,*,#5297,.T.);
#7225=ORIENTED_EDGE('',*,*,#5308,.T.);
#7226=ORIENTED_EDGE('',*,*,#5304,.T.);
#7227=ORIENTED_EDGE('',*,*,#5315,.F.);
#7228=ORIENTED_EDGE('',*,*,#5298,.T.);
#7229=ORIENTED_EDGE('',*,*,#5315,.T.);
#7230=ORIENTED_EDGE('',*,*,#5303,.T.);
#7231=ORIENTED_EDGE('',*,*,#5314,.F.);
#7232=ORIENTED_EDGE('',*,*,#5299,.T.);
#7233=ORIENTED_EDGE('',*,*,#5311,.T.);
#7234=ORIENTED_EDGE('',*,*,#5294,.T.);
#7235=ORIENTED_EDGE('',*,*,#5313,.F.);
#7399=CYLINDRICAL_SURFACE('',#9353,0.25175);
#7864=ADVANCED_FACE('',(#1582),#449,.T.);
#7865=ADVANCED_FACE('',(#1583),#450,.T.);
#7866=ADVANCED_FACE('',(#1584),#1110,.T.);
#7867=ADVANCED_FACE('',(#1585),#1111,.T.);
#7868=ADVANCED_FACE('',(#1586),#1112,.T.);
#7869=ADVANCED_FACE('',(#1587),#7399,.F.);
#7870=ADVANCED_FACE('',(#1588),#1113,.T.);
#7871=ADVANCED_FACE('',(#1589),#1114,.T.);
#7872=ADVANCED_FACE('',(#1590),#1115,.T.);
#7873=ADVANCED_FACE('',(#1591,#823),#1116,.T.);
#7874=ADVANCED_FACE('',(#1592,#824),#1117,.F.);
#7920=CLOSED_SHELL('',(#7864,#7865,#7866,#7867,#7868,#7869,#7870,#7871,
#7872,#7873,#7874));
#9345=AXIS2_PLACEMENT_3D('',#14200,#11839,#11840);
#9346=AXIS2_PLACEMENT_3D('',#14201,#11841,#11842);
#9347=AXIS2_PLACEMENT_3D('',#14213,#11844,#11845);
#9348=AXIS2_PLACEMENT_3D('',#14229,#11846,#11847);
#9349=AXIS2_PLACEMENT_3D('',#14231,#11848,#11849);
#9350=AXIS2_PLACEMENT_3D('',#14257,#11851,#11852);
#9351=AXIS2_PLACEMENT_3D('',#14260,#11855,#11856);
#9352=AXIS2_PLACEMENT_3D('',#14262,#11858,#11859);
#9353=AXIS2_PLACEMENT_3D('',#14264,#11861,#11862);
#9354=AXIS2_PLACEMENT_3D('',#14266,#11863,#11864);
#9355=AXIS2_PLACEMENT_3D('',#14269,#11866,#11867);
#9356=AXIS2_PLACEMENT_3D('',#14270,#11868,#11869);
#9357=AXIS2_PLACEMENT_3D('',#14272,#11871,#11872);
#9358=AXIS2_PLACEMENT_3D('',#14274,#11874,#11875);
#9359=AXIS2_PLACEMENT_3D('',#14275,#11876,#11877);
#9360=AXIS2_PLACEMENT_3D('',#14276,#11878,#11879);
#11839=DIRECTION('axis',(0.,0.,1.));
#11840=DIRECTION('refdir',(1.,0.,0.));
#11841=DIRECTION('center_axis',(0.,1.,0.));
#11842=DIRECTION('ref_axis',(1.,0.,0.));
#11843=DIRECTION('',(0.866025403784439,-0.5,1.06057523872491E-16));
#11844=DIRECTION('center_axis',(0.,-1.,0.));
#11845=DIRECTION('ref_axis',(1.,0.,0.));
#11846=DIRECTION('center_axis',(0.,-1.,0.));
#11847=DIRECTION('ref_axis',(1.,0.,0.));
#11848=DIRECTION('center_axis',(0.,1.,0.));
#11849=DIRECTION('ref_axis',(1.,0.,0.));
#11850=DIRECTION('',(-0.866025403784439,-0.5,-1.06057523872491E-16));
#11851=DIRECTION('center_axis',(1.92296268638356E-16,0.,-1.));
#11852=DIRECTION('ref_axis',(-1.,0.,-1.92296268638356E-16));
#11853=DIRECTION('',(0.,1.,0.));
#11854=DIRECTION('',(0.,1.,0.));
#11855=DIRECTION('center_axis',(-0.866025403784439,0.,-0.5));
#11856=DIRECTION('ref_axis',(-0.5,0.,0.866025403784439));
#11857=DIRECTION('',(0.,1.,0.));
#11858=DIRECTION('center_axis',(-0.866025403784439,0.,0.5));
#11859=DIRECTION('ref_axis',(0.5,0.,0.866025403784439));
#11860=DIRECTION('',(0.,1.,0.));
#11861=DIRECTION('center_axis',(0.,1.,0.));
#11862=DIRECTION('ref_axis',(1.,0.,0.));
#11863=DIRECTION('center_axis',(0.,1.,0.));
#11864=DIRECTION('ref_axis',(1.,0.,0.));
#11865=DIRECTION('',(0.,-1.,0.));
#11866=DIRECTION('center_axis',(0.,1.,0.));
#11867=DIRECTION('ref_axis',(1.,0.,0.));
#11868=DIRECTION('center_axis',(-1.92296268638356E-16,0.,1.));
#11869=DIRECTION('ref_axis',(1.,0.,1.92296268638356E-16));
#11870=DIRECTION('',(0.,1.,0.));
#11871=DIRECTION('center_axis',(0.866025403784439,0.,-0.5));
#11872=DIRECTION('ref_axis',(-0.5,0.,-0.866025403784439));
#11873=DIRECTION('',(0.,1.,0.));
#11874=DIRECTION('center_axis',(0.866025403784439,0.,0.5));
#11875=DIRECTION('ref_axis',(0.5,0.,-0.866025403784439));
#11876=DIRECTION('center_axis',(0.,1.,0.));
#11877=DIRECTION('ref_axis',(1.,0.,0.));
#11878=DIRECTION('center_axis',(0.,1.,0.));
#11879=DIRECTION('ref_axis',(1.,0.,0.));
#14200=CARTESIAN_POINT('',(0.,0.,0.));
#14201=CARTESIAN_POINT('Origin',(0.,0.0584134911936118,0.));
#14202=CARTESIAN_POINT('',(-0.288675134594813,0.0590919554682611,0.5));
#14203=CARTESIAN_POINT('',(0.288675134594813,0.0590919554682611,0.5));
#14204=CARTESIAN_POINT('Ctrl Pts',(-0.288675134594813,0.0590919554682611,
0.5));
#14205=CARTESIAN_POINT('Ctrl Pts',(2.1664336991023E-12,-0.0242413778636964,
0.5));
#14206=CARTESIAN_POINT('Ctrl Pts',(0.288675134594813,0.0590919554682611,
0.5));
#14207=CARTESIAN_POINT('',(-0.577350269189626,0.0590919554682611,-7.07050159149938E-17));
#14208=CARTESIAN_POINT('Ctrl Pts',(-0.577350269189626,0.0590919554682611,
-7.07050159149938E-17));
#14209=CARTESIAN_POINT('Ctrl Pts',(-0.433012701891136,-0.0242413778636963,
0.250000000001876));
#14210=CARTESIAN_POINT('Ctrl Pts',(-0.288675134594813,0.0590919554682611,
0.5));
#14211=CARTESIAN_POINT('',(-0.475,-4.16333634234434E-17,-5.81707229594993E-17));
#14212=CARTESIAN_POINT('',(-0.576175134594813,0.0584134911936118,-7.05611034329833E-17));
#14213=CARTESIAN_POINT('Origin',(0.,0.,0.));
#14214=CARTESIAN_POINT('',(-0.288675134594813,0.0590919554682611,-0.5));
#14215=CARTESIAN_POINT('Ctrl Pts',(-0.288675134594813,0.0590919554682611,
-0.5));
#14216=CARTESIAN_POINT('Ctrl Pts',(-0.433012701893303,-0.0242413778636963,
-0.249999999998124));
#14217=CARTESIAN_POINT('Ctrl Pts',(-0.577350269189626,0.0590919554682611,
-7.07050159149938E-17));
#14218=CARTESIAN_POINT('',(0.288675134594813,0.0590919554682611,-0.5));
#14219=CARTESIAN_POINT('Ctrl Pts',(0.288675134594813,0.0590919554682611,
-0.5));
#14220=CARTESIAN_POINT('Ctrl Pts',(-2.16648921025353E-12,-0.0242413778636962,
-0.5));
#14221=CARTESIAN_POINT('Ctrl Pts',(-0.288675134594813,0.0590919554682611,
-0.5));
#14222=CARTESIAN_POINT('',(0.577350269189626,0.0590919554682611,0.));
#14223=CARTESIAN_POINT('Ctrl Pts',(0.577350269189626,0.0590919554682611,
0.));
#14224=CARTESIAN_POINT('Ctrl Pts',(0.433012701891136,-0.0242413778636963,
-0.250000000001876));
#14225=CARTESIAN_POINT('Ctrl Pts',(0.288675134594813,0.0590919554682611,
-0.5));
#14226=CARTESIAN_POINT('Ctrl Pts',(0.288675134594813,0.0590919554682611,
0.5));
#14227=CARTESIAN_POINT('Ctrl Pts',(0.433012701893303,-0.0242413778636962,
0.249999999998124));
#14228=CARTESIAN_POINT('Ctrl Pts',(0.577350269189626,0.0590919554682611,
0.));
#14229=CARTESIAN_POINT('Origin',(0.,0.461586508806388,0.));
#14230=CARTESIAN_POINT('',(-0.475,0.52,-5.81707229594993E-17));
#14231=CARTESIAN_POINT('Origin',(0.,0.52,0.));
#14232=CARTESIAN_POINT('',(-0.577350269189626,0.460908044531739,-7.07050159149938E-17));
#14233=CARTESIAN_POINT('',(-0.576175134594813,0.461586508806388,-7.05611034329833E-17));
#14234=CARTESIAN_POINT('',(-0.288675134594813,0.460908044531739,0.5));
#14235=CARTESIAN_POINT('Ctrl Pts',(-0.288675134594813,0.460908044531739,
0.5));
#14236=CARTESIAN_POINT('Ctrl Pts',(-0.433012701893303,0.544241377863696,
0.249999999998124));
#14237=CARTESIAN_POINT('Ctrl Pts',(-0.577350269189626,0.460908044531739,
-7.07050159149938E-17));
#14238=CARTESIAN_POINT('',(0.288675134594813,0.460908044531739,0.5));
#14239=CARTESIAN_POINT('Ctrl Pts',(0.288675134594813,0.460908044531739,
0.5));
#14240=CARTESIAN_POINT('Ctrl Pts',(-2.16676676600969E-12,0.544241377863697,
0.5));
#14241=CARTESIAN_POINT('Ctrl Pts',(-0.288675134594813,0.460908044531739,
0.5));
#14242=CARTESIAN_POINT('',(0.577350269189626,0.460908044531739,0.));
#14243=CARTESIAN_POINT('Ctrl Pts',(0.577350269189626,0.460908044531739,
0.));
#14244=CARTESIAN_POINT('Ctrl Pts',(0.433012701891136,0.544241377863696,
0.250000000001876));
#14245=CARTESIAN_POINT('Ctrl Pts',(0.288675134594813,0.460908044531739,
0.5));
#14246=CARTESIAN_POINT('',(0.288675134594813,0.460908044531739,-0.5));
#14247=CARTESIAN_POINT('Ctrl Pts',(0.288675134594813,0.460908044531739,
-0.5));
#14248=CARTESIAN_POINT('Ctrl Pts',(0.433012701893302,0.544241377863696,
-0.249999999998124));
#14249=CARTESIAN_POINT('Ctrl Pts',(0.577350269189626,0.460908044531739,
0.));
#14250=CARTESIAN_POINT('',(-0.288675134594813,0.460908044531739,-0.5));
#14251=CARTESIAN_POINT('Ctrl Pts',(-0.288675134594813,0.460908044531739,
-0.5));
#14252=CARTESIAN_POINT('Ctrl Pts',(2.16660023255599E-12,0.544241377863697,
-0.5));
#14253=CARTESIAN_POINT('Ctrl Pts',(0.288675134594813,0.460908044531739,
-0.5));
#14254=CARTESIAN_POINT('Ctrl Pts',(-0.577350269189626,0.460908044531739,
-7.07050159149938E-17));
#14255=CARTESIAN_POINT('Ctrl Pts',(-0.433012701891136,0.544241377863696,
-0.250000000001876));
#14256=CARTESIAN_POINT('Ctrl Pts',(-0.288675134594813,0.460908044531739,
-0.5));
#14257=CARTESIAN_POINT('Origin',(0.288675134594813,0.,-0.5));
#14258=CARTESIAN_POINT('',(-0.288675134594813,0.,-0.5));
#14259=CARTESIAN_POINT('',(0.288675134594813,0.,-0.5));
#14260=CARTESIAN_POINT('Origin',(-0.288675134594813,0.,-0.5));
#14261=CARTESIAN_POINT('',(-0.577350269189626,0.,-7.07050159149938E-17));
#14262=CARTESIAN_POINT('Origin',(-0.577350269189626,0.,-7.07050159149938E-17));
#14263=CARTESIAN_POINT('',(-0.288675134594813,0.,0.5));
#14264=CARTESIAN_POINT('Origin',(0.,0.,0.));
#14265=CARTESIAN_POINT('',(-0.25175,0.52,3.08304831685346E-17));
#14266=CARTESIAN_POINT('Origin',(0.,0.52,0.));
#14267=CARTESIAN_POINT('',(-0.25175,0.,3.08304831685346E-17));
#14268=CARTESIAN_POINT('',(-0.25175,0.,3.08304831685346E-17));
#14269=CARTESIAN_POINT('Origin',(0.,0.,0.));
#14270=CARTESIAN_POINT('Origin',(-0.288675134594813,0.,0.5));
#14271=CARTESIAN_POINT('',(0.288675134594813,0.,0.5));
#14272=CARTESIAN_POINT('Origin',(0.577350269189626,0.,0.));
#14273=CARTESIAN_POINT('',(0.577350269189626,0.,0.));
#14274=CARTESIAN_POINT('Origin',(0.288675134594813,0.,0.5));
#14275=CARTESIAN_POINT('Origin',(0.,0.52,0.));
#14276=CARTESIAN_POINT('Origin',(0.,0.,0.));
#14343=UNCERTAINTY_MEASURE_WITH_UNIT(LENGTH_MEASURE(0.001),#14393,
'DISTANCE_ACCURACY_VALUE',
'Maximum model space distance between geometric entities at asserted c
onnectivities');
#14344=UNCERTAINTY_MEASURE_WITH_UNIT(LENGTH_MEASURE(0.001),#14393,
'DISTANCE_ACCURACY_VALUE',
'Maximum model space distance between geometric entities at asserted c
onnectivities');
#14391=(
GEOMETRIC_REPRESENTATION_CONTEXT(3)
GLOBAL_UNCERTAINTY_ASSIGNED_CONTEXT((#14343))
GLOBAL_UNIT_ASSIGNED_CONTEXT((#14393,#14395,#14396))
REPRESENTATION_CONTEXT('','3D')
);
#14392=(
GEOMETRIC_REPRESENTATION_CONTEXT(3)
GLOBAL_UNCERTAINTY_ASSIGNED_CONTEXT((#14344))
GLOBAL_UNIT_ASSIGNED_CONTEXT((#14393,#14395,#14396))
REPRESENTATION_CONTEXT('','3D')
);
#14393=(
LENGTH_UNIT()
NAMED_UNIT(*)
SI_UNIT(.CENTI.,.METRE.)
);
#14395=(
NAMED_UNIT(*)
PLANE_ANGLE_UNIT()
SI_UNIT($,.RADIAN.)
);
#14396=(
NAMED_UNIT(*)
SI_UNIT($,.STERADIAN.)
SOLID_ANGLE_UNIT()
);
#14443=SHAPE_DEFINITION_REPRESENTATION(#14562,#14629);
#14562=PRODUCT_DEFINITION_SHAPE('',$,#14677);
#14629=SHAPE_REPRESENTATION('',(#9345),#14391);
#14630=PRODUCT_DEFINITION_CONTEXT('part definition',#14773,'design');
#14677=PRODUCT_DEFINITION('Hex Nut - M6','Hex Nut - M6',#14724,#14630);
#14724=PRODUCT_DEFINITION_FORMATION('',$,#14821);
#14773=APPLICATION_CONTEXT(
'Core Data for Automotive Mechanical Design Process');
#14774=PRODUCT_CONTEXT('part definition',#14773,'mechanical');
#14821=PRODUCT('Hex Nut - M6','Hex Nut - M6','Hex Nut - M6',(#14774));
#14892=COLOUR_RGB('Black',0.12,0.14,0.17);
#14893=FILL_AREA_STYLE_COLOUR('',#14892);
#14894=FILL_AREA_STYLE('',(#14893));
#14895=SURFACE_STYLE_FILL_AREA(#14894);
#14896=SURFACE_SIDE_STYLE('',(#14895));
#14897=SURFACE_STYLE_USAGE(.BOTH.,#14896);
#14898=PRESENTATION_STYLE_ASSIGNMENT((#14897));
ENDSEC;
END-ISO-10303-21;
